ISO-10303-21;
HEADER;
/* Generated by software containing ST-Developer
 * from STEP Tools, Inc. (www.steptools.com) 
 */

FILE_DESCRIPTION(
/* description */ ('PAT-072'),
/* implementation_level */ '2;1');

FILE_NAME(
/* name */ 'Sight glass gasket.step',
/* time_stamp */ '2026-10-29T20:11:56-07:00',
/* author */ (''),
/* organization */ (''),
/* preprocessor_version */ 'ST-DEVELOPER v20.2',
/* originating_system */ 'Autodesk Translation Framework v15.17.0.0',
/* authorisation */ '');

FILE_SCHEMA (('AUTOMOTIVE_DESIGN { 1 0 10303 214 3 1 1 }'));
ENDSEC;

DATA;
#10=MECHANICAL_DESIGN_GEOMETRIC_PRESENTATION_REPRESENTATION('',(#351),#11432);
#279=SHAPE_REPRESENTATION_RELATIONSHIP('SRR','None',#11583,#315);
#315=ADVANCED_BREP_SHAPE_REPRESENTATION('',(#387),#11414);
#351=STYLED_ITEM('',(#11833),#387);
#387=MANIFOLD_SOLID_BREP('Body1',#6086);
#500=FACE_BOUND('',#1468,.T.);
#501=FACE_BOUND('',#1469,.T.);
#502=FACE_BOUND('',#1470,.T.);
#503=FACE_BOUND('',#1471,.T.);
#504=FACE_BOUND('',#1472,.T.);
#505=FACE_BOUND('',#1475,.T.);
#506=FACE_BOUND('',#1476,.T.);
#507=FACE_BOUND('',#1477,.T.);
#508=FACE_BOUND('',#1478,.T.);
#509=FACE_BOUND('',#1479,.T.);
#676=PLANE('',#6900);
#677=PLANE('',#6901);
#678=PLANE('',#6902);
#679=PLANE('',#6903);
#680=PLANE('',#6904);
#681=PLANE('',#6905);
#682=PLANE('',#6906);
#683=PLANE('',#6907);
#684=PLANE('',#6908);
#685=PLANE('',#6909);
#989=FACE_OUTER_BOUND('',#1459,.T.);
#990=FACE_OUTER_BOUND('',#1460,.T.);
#991=FACE_OUTER_BOUND('',#1461,.T.);
#992=FACE_OUTER_BOUND('',#1462,.T.);
#993=FACE_OUTER_BOUND('',#1463,.T.);
#994=FACE_OUTER_BOUND('',#1464,.T.);
#995=FACE_OUTER_BOUND('',#1465,.T.);
#996=FACE_OUTER_BOUND('',#1466,.T.);
#997=FACE_OUTER_BOUND('',#1467,.T.);
#998=FACE_OUTER_BOUND('',#1473,.T.);
#999=FACE_OUTER_BOUND('',#1474,.T.);
#1000=FACE_OUTER_BOUND('',#1480,.T.);
#1001=FACE_OUTER_BOUND('',#1481,.T.);
#1002=FACE_OUTER_BOUND('',#1482,.T.);
#1459=EDGE_LOOP('',(#4814,#4815,#4816,#4817));
#1460=EDGE_LOOP('',(#4818,#4819,#4820,#4821));
#1461=EDGE_LOOP('',(#4822,#4823,#4824,#4825));
#1462=EDGE_LOOP('',(#4826,#4827,#4828,#4829));
#1463=EDGE_LOOP('',(#4830,#4831,#4832,#4833));
#1464=EDGE_LOOP('',(#4834,#4835,#4836,#4837));
#1465=EDGE_LOOP('',(#4838,#4839,#4840,#4841));
#1466=EDGE_LOOP('',(#4842,#4843,#4844,#4845));
#1467=EDGE_LOOP('',(#4846,#4847,#4848,#4849));
#1468=EDGE_LOOP('',(#4850,#4851,#4852,#4853));
#1469=EDGE_LOOP('',(#4854));
#1470=EDGE_LOOP('',(#4855));
#1471=EDGE_LOOP('',(#4856));
#1472=EDGE_LOOP('',(#4857));
#1473=EDGE_LOOP('',(#4858,#4859,#4860,#4861));
#1474=EDGE_LOOP('',(#4862,#4863,#4864,#4865));
#1475=EDGE_LOOP('',(#4866,#4867,#4868,#4869));
#1476=EDGE_LOOP('',(#4870));
#1477=EDGE_LOOP('',(#4871));
#1478=EDGE_LOOP('',(#4872));
#1479=EDGE_LOOP('',(#4873));
#1480=EDGE_LOOP('',(#4874,#4875,#4876,#4877));
#1481=EDGE_LOOP('',(#4878,#4879,#4880,#4881));
#1482=EDGE_LOOP('',(#4882,#4883,#4884,#4885));
#1880=LINE('',#10496,#2299);
#1881=LINE('',#10502,#2300);
#1882=LINE('',#10508,#2301);
#1883=LINE('',#10514,#2302);
#1884=LINE('',#10519,#2303);
#1885=LINE('',#10521,#2304);
#1886=LINE('',#10523,#2305);
#1887=LINE('',#10524,#2306);
#1888=LINE('',#10527,#2307);
#1889=LINE('',#10529,#2308);
#1890=LINE('',#10530,#2309);
#1891=LINE('',#10533,#2310);
#1892=LINE('',#10535,#2311);
#1893=LINE('',#10536,#2312);
#1894=LINE('',#10538,#2313);
#1895=LINE('',#10539,#2314);
#1896=LINE('',#10543,#2315);
#1897=LINE('',#10545,#2316);
#1898=LINE('',#10547,#2317);
#1899=LINE('',#10548,#2318);
#1900=LINE('',#10551,#2319);
#1901=LINE('',#10553,#2320);
#1902=LINE('',#10554,#2321);
#1903=LINE('',#10557,#2322);
#1904=LINE('',#10559,#2323);
#1905=LINE('',#10560,#2324);
#1906=LINE('',#10562,#2325);
#1907=LINE('',#10563,#2326);
#2299=VECTOR('',#8207,0.12);
#2300=VECTOR('',#8214,0.12);
#2301=VECTOR('',#8221,0.12);
#2302=VECTOR('',#8228,0.12);
#2303=VECTOR('',#8233,1.);
#2304=VECTOR('',#8234,1.);
#2305=VECTOR('',#8235,1.);
#2306=VECTOR('',#8236,1.);
#2307=VECTOR('',#8239,1.);
#2308=VECTOR('',#8240,1.);
#2309=VECTOR('',#8241,1.);
#2310=VECTOR('',#8244,1.);
#2311=VECTOR('',#8245,1.);
#2312=VECTOR('',#8246,1.);
#2313=VECTOR('',#8249,1.);
#2314=VECTOR('',#8250,1.);
#2315=VECTOR('',#8253,1.);
#2316=VECTOR('',#8254,1.);
#2317=VECTOR('',#8255,1.);
#2318=VECTOR('',#8256,1.);
#2319=VECTOR('',#8259,1.);
#2320=VECTOR('',#8260,1.);
#2321=VECTOR('',#8261,1.);
#2322=VECTOR('',#8264,1.);
#2323=VECTOR('',#8265,1.);
#2324=VECTOR('',#8266,1.);
#2325=VECTOR('',#8269,1.);
#2326=VECTOR('',#8270,1.);
#2711=CIRCLE('',#6889,0.12);
#2712=CIRCLE('',#6890,0.12);
#2713=CIRCLE('',#6892,0.12);
#2714=CIRCLE('',#6893,0.12);
#2715=CIRCLE('',#6895,0.12);
#2716=CIRCLE('',#6896,0.12);
#2717=CIRCLE('',#6898,0.12);
#2718=CIRCLE('',#6899,0.12);
#3078=VERTEX_POINT('',#10493);
#3079=VERTEX_POINT('',#10495);
#3080=VERTEX_POINT('',#10499);
#3081=VERTEX_POINT('',#10501);
#3082=VERTEX_POINT('',#10505);
#3083=VERTEX_POINT('',#10507);
#3084=VERTEX_POINT('',#10511);
#3085=VERTEX_POINT('',#10513);
#3086=VERTEX_POINT('',#10517);
#3087=VERTEX_POINT('',#10518);
#3088=VERTEX_POINT('',#10520);
#3089=VERTEX_POINT('',#10522);
#3090=VERTEX_POINT('',#10526);
#3091=VERTEX_POINT('',#10528);
#3092=VERTEX_POINT('',#10532);
#3093=VERTEX_POINT('',#10534);
#3094=VERTEX_POINT('',#10541);
#3095=VERTEX_POINT('',#10542);
#3096=VERTEX_POINT('',#10544);
#3097=VERTEX_POINT('',#10546);
#3098=VERTEX_POINT('',#10550);
#3099=VERTEX_POINT('',#10552);
#3100=VERTEX_POINT('',#10556);
#3101=VERTEX_POINT('',#10558);
#3696=EDGE_CURVE('',#3078,#3078,#2711,.T.);
#3697=EDGE_CURVE('',#3078,#3079,#1880,.T.);
#3698=EDGE_CURVE('',#3079,#3079,#2712,.T.);
#3699=EDGE_CURVE('',#3080,#3080,#2713,.T.);
#3700=EDGE_CURVE('',#3080,#3081,#1881,.T.);
#3701=EDGE_CURVE('',#3081,#3081,#2714,.T.);
#3702=EDGE_CURVE('',#3082,#3082,#2715,.T.);
#3703=EDGE_CURVE('',#3082,#3083,#1882,.T.);
#3704=EDGE_CURVE('',#3083,#3083,#2716,.T.);
#3705=EDGE_CURVE('',#3084,#3084,#2717,.T.);
#3706=EDGE_CURVE('',#3084,#3085,#1883,.T.);
#3707=EDGE_CURVE('',#3085,#3085,#2718,.T.);
#3708=EDGE_CURVE('',#3086,#3087,#1884,.T.);
#3709=EDGE_CURVE('',#3088,#3086,#1885,.T.);
#3710=EDGE_CURVE('',#3089,#3088,#1886,.T.);
#3711=EDGE_CURVE('',#3089,#3087,#1887,.T.);
#3712=EDGE_CURVE('',#3087,#3090,#1888,.T.);
#3713=EDGE_CURVE('',#3091,#3089,#1889,.T.);
#3714=EDGE_CURVE('',#3091,#3090,#1890,.T.);
#3715=EDGE_CURVE('',#3090,#3092,#1891,.T.);
#3716=EDGE_CURVE('',#3093,#3091,#1892,.T.);
#3717=EDGE_CURVE('',#3093,#3092,#1893,.T.);
#3718=EDGE_CURVE('',#3092,#3086,#1894,.T.);
#3719=EDGE_CURVE('',#3088,#3093,#1895,.T.);
#3720=EDGE_CURVE('',#3094,#3095,#1896,.T.);
#3721=EDGE_CURVE('',#3095,#3096,#1897,.T.);
#3722=EDGE_CURVE('',#3097,#3096,#1898,.T.);
#3723=EDGE_CURVE('',#3094,#3097,#1899,.T.);
#3724=EDGE_CURVE('',#3098,#3094,#1900,.T.);
#3725=EDGE_CURVE('',#3099,#3097,#1901,.T.);
#3726=EDGE_CURVE('',#3098,#3099,#1902,.T.);
#3727=EDGE_CURVE('',#3100,#3098,#1903,.T.);
#3728=EDGE_CURVE('',#3101,#3099,#1904,.T.);
#3729=EDGE_CURVE('',#3100,#3101,#1905,.T.);
#3730=EDGE_CURVE('',#3095,#3100,#1906,.T.);
#3731=EDGE_CURVE('',#3096,#3101,#1907,.T.);
#4814=ORIENTED_EDGE('',*,*,#3696,.F.);
#4815=ORIENTED_EDGE('',*,*,#3697,.T.);
#4816=ORIENTED_EDGE('',*,*,#3698,.F.);
#4817=ORIENTED_EDGE('',*,*,#3697,.F.);
#4818=ORIENTED_EDGE('',*,*,#3699,.F.);
#4819=ORIENTED_EDGE('',*,*,#3700,.T.);
#4820=ORIENTED_EDGE('',*,*,#3701,.F.);
#4821=ORIENTED_EDGE('',*,*,#3700,.F.);
#4822=ORIENTED_EDGE('',*,*,#3702,.F.);
#4823=ORIENTED_EDGE('',*,*,#3703,.T.);
#4824=ORIENTED_EDGE('',*,*,#3704,.F.);
#4825=ORIENTED_EDGE('',*,*,#3703,.F.);
#4826=ORIENTED_EDGE('',*,*,#3705,.F.);
#4827=ORIENTED_EDGE('',*,*,#3706,.T.);
#4828=ORIENTED_EDGE('',*,*,#3707,.F.);
#4829=ORIENTED_EDGE('',*,*,#3706,.F.);
#4830=ORIENTED_EDGE('',*,*,#3708,.F.);
#4831=ORIENTED_EDGE('',*,*,#3709,.F.);
#4832=ORIENTED_EDGE('',*,*,#3710,.F.);
#4833=ORIENTED_EDGE('',*,*,#3711,.T.);
#4834=ORIENTED_EDGE('',*,*,#3712,.F.);
#4835=ORIENTED_EDGE('',*,*,#3711,.F.);
#4836=ORIENTED_EDGE('',*,*,#3713,.F.);
#4837=ORIENTED_EDGE('',*,*,#3714,.T.);
#4838=ORIENTED_EDGE('',*,*,#3715,.F.);
#4839=ORIENTED_EDGE('',*,*,#3714,.F.);
#4840=ORIENTED_EDGE('',*,*,#3716,.F.);
#4841=ORIENTED_EDGE('',*,*,#3717,.T.);
#4842=ORIENTED_EDGE('',*,*,#3718,.F.);
#4843=ORIENTED_EDGE('',*,*,#3717,.F.);
#4844=ORIENTED_EDGE('',*,*,#3719,.F.);
#4845=ORIENTED_EDGE('',*,*,#3709,.T.);
#4846=ORIENTED_EDGE('',*,*,#3720,.T.);
#4847=ORIENTED_EDGE('',*,*,#3721,.T.);
#4848=ORIENTED_EDGE('',*,*,#3722,.F.);
#4849=ORIENTED_EDGE('',*,*,#3723,.F.);
#4850=ORIENTED_EDGE('',*,*,#3715,.T.);
#4851=ORIENTED_EDGE('',*,*,#3718,.T.);
#4852=ORIENTED_EDGE('',*,*,#3708,.T.);
#4853=ORIENTED_EDGE('',*,*,#3712,.T.);
#4854=ORIENTED_EDGE('',*,*,#3707,.T.);
#4855=ORIENTED_EDGE('',*,*,#3704,.T.);
#4856=ORIENTED_EDGE('',*,*,#3701,.T.);
#4857=ORIENTED_EDGE('',*,*,#3698,.T.);
#4858=ORIENTED_EDGE('',*,*,#3724,.T.);
#4859=ORIENTED_EDGE('',*,*,#3723,.T.);
#4860=ORIENTED_EDGE('',*,*,#3725,.F.);
#4861=ORIENTED_EDGE('',*,*,#3726,.F.);
#4862=ORIENTED_EDGE('',*,*,#3727,.T.);
#4863=ORIENTED_EDGE('',*,*,#3726,.T.);
#4864=ORIENTED_EDGE('',*,*,#3728,.F.);
#4865=ORIENTED_EDGE('',*,*,#3729,.F.);
#4866=ORIENTED_EDGE('',*,*,#3716,.T.);
#4867=ORIENTED_EDGE('',*,*,#3713,.T.);
#4868=ORIENTED_EDGE('',*,*,#3710,.T.);
#4869=ORIENTED_EDGE('',*,*,#3719,.T.);
#4870=ORIENTED_EDGE('',*,*,#3705,.T.);
#4871=ORIENTED_EDGE('',*,*,#3702,.T.);
#4872=ORIENTED_EDGE('',*,*,#3699,.T.);
#4873=ORIENTED_EDGE('',*,*,#3696,.T.);
#4874=ORIENTED_EDGE('',*,*,#3730,.T.);
#4875=ORIENTED_EDGE('',*,*,#3729,.T.);
#4876=ORIENTED_EDGE('',*,*,#3731,.F.);
#4877=ORIENTED_EDGE('',*,*,#3721,.F.);
#4878=ORIENTED_EDGE('',*,*,#3731,.T.);
#4879=ORIENTED_EDGE('',*,*,#3728,.T.);
#4880=ORIENTED_EDGE('',*,*,#3725,.T.);
#4881=ORIENTED_EDGE('',*,*,#3722,.T.);
#4882=ORIENTED_EDGE('',*,*,#3730,.F.);
#4883=ORIENTED_EDGE('',*,*,#3720,.F.);
#4884=ORIENTED_EDGE('',*,*,#3724,.F.);
#4885=ORIENTED_EDGE('',*,*,#3727,.F.);
#5645=CYLINDRICAL_SURFACE('',#6888,0.12);
#5646=CYLINDRICAL_SURFACE('',#6891,0.12);
#5647=CYLINDRICAL_SURFACE('',#6894,0.12);
#5648=CYLINDRICAL_SURFACE('',#6897,0.12);
#5888=ADVANCED_FACE('',(#989),#5645,.F.);
#5889=ADVANCED_FACE('',(#990),#5646,.F.);
#5890=ADVANCED_FACE('',(#991),#5647,.F.);
#5891=ADVANCED_FACE('',(#992),#5648,.F.);
#5892=ADVANCED_FACE('',(#993),#676,.F.);
#5893=ADVANCED_FACE('',(#994),#677,.F.);
#5894=ADVANCED_FACE('',(#995),#678,.F.);
#5895=ADVANCED_FACE('',(#996),#679,.F.);
#5896=ADVANCED_FACE('',(#997,#500,#501,#502,#503,#504),#680,.T.);
#5897=ADVANCED_FACE('',(#998),#681,.T.);
#5898=ADVANCED_FACE('',(#999,#505,#506,#507,#508,#509),#682,.T.);
#5899=ADVANCED_FACE('',(#1000),#683,.T.);
#5900=ADVANCED_FACE('',(#1001),#684,.T.);
#5901=ADVANCED_FACE('',(#1002),#685,.F.);
#6086=CLOSED_SHELL('',(#5888,#5889,#5890,#5891,#5892,#5893,#5894,#5895,
#5896,#5897,#5898,#5899,#5900,#5901));
#6887=AXIS2_PLACEMENT_3D('',#10491,#8201,#8202);
#6888=AXIS2_PLACEMENT_3D('',#10492,#8203,#8204);
#6889=AXIS2_PLACEMENT_3D('',#10494,#8205,#8206);
#6890=AXIS2_PLACEMENT_3D('',#10497,#8208,#8209);
#6891=AXIS2_PLACEMENT_3D('',#10498,#8210,#8211);
#6892=AXIS2_PLACEMENT_3D('',#10500,#8212,#8213);
#6893=AXIS2_PLACEMENT_3D('',#10503,#8215,#8216);
#6894=AXIS2_PLACEMENT_3D('',#10504,#8217,#8218);
#6895=AXIS2_PLACEMENT_3D('',#10506,#8219,#8220);
#6896=AXIS2_PLACEMENT_3D('',#10509,#8222,#8223);
#6897=AXIS2_PLACEMENT_3D('',#10510,#8224,#8225);
#6898=AXIS2_PLACEMENT_3D('',#10512,#8226,#8227);
#6899=AXIS2_PLACEMENT_3D('',#10515,#8229,#8230);
#6900=AXIS2_PLACEMENT_3D('',#10516,#8231,#8232);
#6901=AXIS2_PLACEMENT_3D('',#10525,#8237,#8238);
#6902=AXIS2_PLACEMENT_3D('',#10531,#8242,#8243);
#6903=AXIS2_PLACEMENT_3D('',#10537,#8247,#8248);
#6904=AXIS2_PLACEMENT_3D('',#10540,#8251,#8252);
#6905=AXIS2_PLACEMENT_3D('',#10549,#8257,#8258);
#6906=AXIS2_PLACEMENT_3D('',#10555,#8262,#8263);
#6907=AXIS2_PLACEMENT_3D('',#10561,#8267,#8268);
#6908=AXIS2_PLACEMENT_3D('',#10564,#8271,#8272);
#6909=AXIS2_PLACEMENT_3D('',#10565,#8273,#8274);
#8201=DIRECTION('axis',(0.,0.,1.));
#8202=DIRECTION('refdir',(1.,0.,0.));
#8203=DIRECTION('center_axis',(0.,1.,0.));
#8204=DIRECTION('ref_axis',(1.,0.,0.));
#8205=DIRECTION('center_axis',(0.,1.,0.));
#8206=DIRECTION('ref_axis',(1.,0.,0.));
#8207=DIRECTION('',(0.,1.,0.));
#8208=DIRECTION('center_axis',(0.,-1.,0.));
#8209=DIRECTION('ref_axis',(1.,0.,0.));
#8210=DIRECTION('center_axis',(0.,1.,0.));
#8211=DIRECTION('ref_axis',(1.,0.,0.));
#8212=DIRECTION('center_axis',(0.,1.,0.));
#8213=DIRECTION('ref_axis',(1.,0.,0.));
#8214=DIRECTION('',(0.,1.,0.));
#8215=DIRECTION('center_axis',(0.,-1.,0.));
#8216=DIRECTION('ref_axis',(1.,0.,0.));
#8217=DIRECTION('center_axis',(0.,1.,0.));
#8218=DIRECTION('ref_axis',(1.,0.,0.));
#8219=DIRECTION('center_axis',(0.,1.,0.));
#8220=DIRECTION('ref_axis',(1.,0.,0.));
#8221=DIRECTION('',(0.,1.,0.));
#8222=DIRECTION('center_axis',(0.,-1.,0.));
#8223=DIRECTION('ref_axis',(1.,0.,0.));
#8224=DIRECTION('center_axis',(0.,1.,0.));
#8225=DIRECTION('ref_axis',(1.,0.,0.));
#8226=DIRECTION('center_axis',(0.,1.,0.));
#8227=DIRECTION('ref_axis',(1.,0.,0.));
#8228=DIRECTION('',(0.,1.,0.));
#8229=DIRECTION('center_axis',(0.,-1.,0.));
#8230=DIRECTION('ref_axis',(1.,0.,0.));
#8231=DIRECTION('center_axis',(1.,0.,0.));
#8232=DIRECTION('ref_axis',(0.,0.,-1.));
#8233=DIRECTION('',(0.,0.,1.));
#8234=DIRECTION('',(0.,1.,0.));
#8235=DIRECTION('',(0.,0.,-1.));
#8236=DIRECTION('',(0.,1.,0.));
#8237=DIRECTION('center_axis',(0.,0.,1.));
#8238=DIRECTION('ref_axis',(1.,0.,0.));
#8239=DIRECTION('',(-1.,0.,0.));
#8240=DIRECTION('',(1.,0.,0.));
#8241=DIRECTION('',(0.,1.,0.));
#8242=DIRECTION('center_axis',(-1.,0.,0.));
#8243=DIRECTION('ref_axis',(0.,0.,1.));
#8244=DIRECTION('',(0.,0.,-1.));
#8245=DIRECTION('',(0.,0.,1.));
#8246=DIRECTION('',(0.,1.,0.));
#8247=DIRECTION('center_axis',(0.,0.,-1.));
#8248=DIRECTION('ref_axis',(-1.,0.,0.));
#8249=DIRECTION('',(1.,0.,0.));
#8250=DIRECTION('',(-1.,0.,0.));
#8251=DIRECTION('center_axis',(0.,1.,0.));
#8252=DIRECTION('ref_axis',(-1.,0.,0.));
#8253=DIRECTION('',(-1.,0.,0.));
#8254=DIRECTION('',(0.,0.,1.));
#8255=DIRECTION('',(-1.,0.,0.));
#8256=DIRECTION('',(0.,0.,1.));
#8257=DIRECTION('center_axis',(1.,0.,0.));
#8258=DIRECTION('ref_axis',(0.,1.,0.));
#8259=DIRECTION('',(0.,1.,0.));
#8260=DIRECTION('',(0.,1.,0.));
#8261=DIRECTION('',(0.,0.,1.));
#8262=DIRECTION('center_axis',(0.,-1.,0.));
#8263=DIRECTION('ref_axis',(1.,0.,0.));
#8264=DIRECTION('',(1.,0.,0.));
#8265=DIRECTION('',(1.,0.,0.));
#8266=DIRECTION('',(0.,0.,1.));
#8267=DIRECTION('center_axis',(-1.,0.,0.));
#8268=DIRECTION('ref_axis',(0.,-1.,0.));
#8269=DIRECTION('',(0.,-1.,0.));
#8270=DIRECTION('',(0.,-1.,0.));
#8271=DIRECTION('center_axis',(0.,0.,1.));
#8272=DIRECTION('ref_axis',(1.,0.,0.));
#8273=DIRECTION('center_axis',(0.,0.,1.));
#8274=DIRECTION('ref_axis',(1.,0.,0.));
#10491=CARTESIAN_POINT('',(0.,0.,0.));
#10492=CARTESIAN_POINT('Origin',(0.8,-3.2,9.8));
#10493=CARTESIAN_POINT('',(0.68,-2.7,9.8));
#10494=CARTESIAN_POINT('Origin',(0.8,-2.7,9.8));
#10495=CARTESIAN_POINT('',(0.68,-2.5,9.8));
#10496=CARTESIAN_POINT('',(0.68,-3.2,9.8));
#10497=CARTESIAN_POINT('Origin',(0.8,-2.5,9.8));
#10498=CARTESIAN_POINT('Origin',(-0.8,-3.2,13.2));
#10499=CARTESIAN_POINT('',(-0.92,-2.7,13.2));
#10500=CARTESIAN_POINT('Origin',(-0.8,-2.7,13.2));
#10501=CARTESIAN_POINT('',(-0.92,-2.5,13.2));
#10502=CARTESIAN_POINT('',(-0.92,-3.2,13.2));
#10503=CARTESIAN_POINT('Origin',(-0.8,-2.5,13.2));
#10504=CARTESIAN_POINT('Origin',(-0.8,-3.2,9.8));
#10505=CARTESIAN_POINT('',(-0.92,-2.7,9.8));
#10506=CARTESIAN_POINT('Origin',(-0.8,-2.7,9.8));
#10507=CARTESIAN_POINT('',(-0.92,-2.5,9.8));
#10508=CARTESIAN_POINT('',(-0.92,-3.2,9.8));
#10509=CARTESIAN_POINT('Origin',(-0.8,-2.5,9.8));
#10510=CARTESIAN_POINT('Origin',(0.8,-3.2,13.2));
#10511=CARTESIAN_POINT('',(0.68,-2.7,13.2));
#10512=CARTESIAN_POINT('Origin',(0.8,-2.7,13.2));
#10513=CARTESIAN_POINT('',(0.68,-2.5,13.2));
#10514=CARTESIAN_POINT('',(0.68,-3.2,13.2));
#10515=CARTESIAN_POINT('Origin',(0.8,-2.5,13.2));
#10516=CARTESIAN_POINT('Origin',(0.6,-2.8,13.));
#10517=CARTESIAN_POINT('',(0.6,-2.5,10.));
#10518=CARTESIAN_POINT('',(0.6,-2.5,13.));
#10519=CARTESIAN_POINT('',(0.6,-2.5,11.25));
#10520=CARTESIAN_POINT('',(0.6,-2.7,10.));
#10521=CARTESIAN_POINT('',(0.6,-2.8,10.));
#10522=CARTESIAN_POINT('',(0.6,-2.7,13.));
#10523=CARTESIAN_POINT('',(0.6,-2.7,11.25));
#10524=CARTESIAN_POINT('',(0.6,-2.8,13.));
#10525=CARTESIAN_POINT('Origin',(-0.6,-2.8,13.));
#10526=CARTESIAN_POINT('',(-0.6,-2.5,13.));
#10527=CARTESIAN_POINT('',(0.2,-2.5,13.));
#10528=CARTESIAN_POINT('',(-0.6,-2.7,13.));
#10529=CARTESIAN_POINT('',(-0.8,-2.7,13.));
#10530=CARTESIAN_POINT('',(-0.6,-2.8,13.));
#10531=CARTESIAN_POINT('Origin',(-0.6,-2.8,10.));
#10532=CARTESIAN_POINT('',(-0.6,-2.5,10.));
#10533=CARTESIAN_POINT('',(-0.6,-2.5,9.75));
#10534=CARTESIAN_POINT('',(-0.6,-2.7,10.));
#10535=CARTESIAN_POINT('',(-0.6,-2.7,9.75));
#10536=CARTESIAN_POINT('',(-0.6,-2.8,10.));
#10537=CARTESIAN_POINT('Origin',(0.6,-2.8,10.));
#10538=CARTESIAN_POINT('',(0.8,-2.5,10.));
#10539=CARTESIAN_POINT('',(-0.2,-2.7,10.));
#10540=CARTESIAN_POINT('Origin',(1.,-2.5,9.5));
#10541=CARTESIAN_POINT('',(1.,-2.5,9.5));
#10542=CARTESIAN_POINT('',(-1.,-2.5,9.5));
#10543=CARTESIAN_POINT('',(1.,-2.5,9.5));
#10544=CARTESIAN_POINT('',(-1.,-2.5,13.5));
#10545=CARTESIAN_POINT('',(-1.,-2.5,9.5));
#10546=CARTESIAN_POINT('',(1.,-2.5,13.5));
#10547=CARTESIAN_POINT('',(1.,-2.5,13.5));
#10548=CARTESIAN_POINT('',(1.,-2.5,9.5));
#10549=CARTESIAN_POINT('Origin',(1.,-2.7,9.5));
#10550=CARTESIAN_POINT('',(1.,-2.7,9.5));
#10551=CARTESIAN_POINT('',(1.,-2.7,9.5));
#10552=CARTESIAN_POINT('',(1.,-2.7,13.5));
#10553=CARTESIAN_POINT('',(1.,-2.7,13.5));
#10554=CARTESIAN_POINT('',(1.,-2.7,9.5));
#10555=CARTESIAN_POINT('Origin',(-1.,-2.7,9.5));
#10556=CARTESIAN_POINT('',(-1.,-2.7,9.5));
#10557=CARTESIAN_POINT('',(-1.,-2.7,9.5));
#10558=CARTESIAN_POINT('',(-1.,-2.7,13.5));
#10559=CARTESIAN_POINT('',(-1.,-2.7,13.5));
#10560=CARTESIAN_POINT('',(-1.,-2.7,9.5));
#10561=CARTESIAN_POINT('Origin',(-1.,-2.5,9.5));
#10562=CARTESIAN_POINT('',(-1.,-2.5,9.5));
#10563=CARTESIAN_POINT('',(-1.,-2.5,13.5));
#10564=CARTESIAN_POINT('Origin',(0.,-2.6,13.5));
#10565=CARTESIAN_POINT('Origin',(0.,-2.6,9.5));
#11375=UNCERTAINTY_MEASURE_WITH_UNIT(LENGTH_MEASURE(0.001),#11433,
'DISTANCE_ACCURACY_VALUE',
'Maximum model space distance between geometric entities at asserted c
onnectivities');
#11393=UNCERTAINTY_MEASURE_WITH_UNIT(LENGTH_MEASURE(0.001),#11433,
'DISTANCE_ACCURACY_VALUE',
'Maximum model space distance between geometric entities at asserted c
onnectivities');
#11414=(
GEOMETRIC_REPRESENTATION_CONTEXT(3)
GLOBAL_UNCERTAINTY_ASSIGNED_CONTEXT((#11375))
GLOBAL_UNIT_ASSIGNED_CONTEXT((#11433,#11435,#11436))
REPRESENTATION_CONTEXT('','3D')
);
#11432=(
GEOMETRIC_REPRESENTATION_CONTEXT(3)
GLOBAL_UNCERTAINTY_ASSIGNED_CONTEXT((#11393))
GLOBAL_UNIT_ASSIGNED_CONTEXT((#11433,#11435,#11436))
REPRESENTATION_CONTEXT('','3D')
);
#11433=(
LENGTH_UNIT()
NAMED_UNIT(*)
SI_UNIT(.CENTI.,.METRE.)
);
#11435=(
NAMED_UNIT(*)
PLANE_ANGLE_UNIT()
SI_UNIT($,.RADIAN.)
);
#11436=(
NAMED_UNIT(*)
SI_UNIT($,.STERADIAN.)
SOLID_ANGLE_UNIT()
);
#11457=SHAPE_DEFINITION_REPRESENTATION(#11495,#11583);
#11495=PRODUCT_DEFINITION_SHAPE('',$,#11622);
#11583=SHAPE_REPRESENTATION('',(#6887),#11414);
#11601=PRODUCT_DEFINITION_CONTEXT('part definition',#11717,'design');
#11622=PRODUCT_DEFINITION('Sight glass gasket',
'Sight glass gasket',#11660,#11601);
#11660=PRODUCT_DEFINITION_FORMATION('',$,#11739);
#11717=APPLICATION_CONTEXT(
'Core Data for Automotive Mechanical Design Process');
#11718=PRODUCT_CONTEXT('part definition',#11717,'mechanical');
#11739=PRODUCT('Sight glass gasket','Sight glass gasket',
'Sight glass gasket',(#11718));
#11827=COLOUR_RGB('Off White',0.89,0.88,0.83);
#11828=FILL_AREA_STYLE_COLOUR('',#11827);
#11829=FILL_AREA_STYLE('',(#11828));
#11830=SURFACE_STYLE_FILL_AREA(#11829);
#11831=SURFACE_SIDE_STYLE('',(#11830));
#11832=SURFACE_STYLE_USAGE(.BOTH.,#11831);
#11833=PRESENTATION_STYLE_ASSIGNMENT((#11832));
ENDSEC;
END-ISO-10303-21;
